ISO-10303-21;
HEADER;
/* Generated by software containing ST-Developer
 * from STEP Tools, Inc. (www.steptools.com) 
 */

FILE_DESCRIPTION(
/* description */ ('CAx-IF Rec.Pracs.---Representation and Presentation of Product Manufa
cturing Information (PMI)---4.0---2014-10-13'),
/* implementation_level */ '2;1');

FILE_NAME(
/* name */ 'Socket Screw 5.step',
/* time_stamp */ '2026-10-24T18:52:33-07:00',
/* author */ (''),
/* organization */ (''),
/* preprocessor_version */ 'ST-DEVELOPER v20.2',
/* originating_system */ 'Autodesk Translation Framework v15.17.0.0',
/* authorisation */ '');

FILE_SCHEMA (('AP242_MANAGED_MODEL_BASED_3D_ENGINEERING_MIM_LF { 1 0 10303 442 2 1 4 }'));
ENDSEC;

DATA;
#10=MECHANICAL_DESIGN_GEOMETRIC_PRESENTATION_REPRESENTATION('',(#437),#34876);
#371=SHAPE_REPRESENTATION_RELATIONSHIP('SRR','None',#35008,#404);
#404=ADVANCED_BREP_SHAPE_REPRESENTATION('',(#470),#34866);
#437=STYLED_ITEM('',(#35159),#470);
#470=MANIFOLD_SOLID_BREP('Socket Screw 5',#19577);
#943=PLANE('',#21749);
#944=PLANE('',#21750);
#945=PLANE('',#21751);
#946=PLANE('',#21752);
#947=PLANE('',#21756);
#948=PLANE('',#21757);
#949=PLANE('',#21758);
#950=PLANE('',#21759);
#2234=LINE('',#33167,#3833);
#2235=LINE('',#33169,#3834);
#2236=LINE('',#33171,#3835);
#2237=LINE('',#33172,#3836);
#2238=LINE('',#33176,#3837);
#2239=LINE('',#33178,#3838);
#2240=LINE('',#33180,#3839);
#2241=LINE('',#33181,#3840);
#2242=LINE('',#33183,#3841);
#2243=LINE('',#33184,#3842);
#2244=LINE('',#33189,#3843);
#2245=LINE('',#33191,#3844);
#2246=LINE('',#33192,#3845);
#2247=LINE('',#33195,#3846);
#2248=LINE('',#33199,#3847);
#2249=LINE('',#33201,#3848);
#2250=LINE('',#33202,#3849);
#2251=LINE('',#33204,#3850);
#2252=LINE('',#33206,#3851);
#3833=VECTOR('',#27007,1.);
#3834=VECTOR('',#27008,1.);
#3835=VECTOR('',#27009,1.);
#3836=VECTOR('',#27010,1.);
#3837=VECTOR('',#27013,1.);
#3838=VECTOR('',#27014,1.);
#3839=VECTOR('',#27015,1.);
#3840=VECTOR('',#27016,1.);
#3841=VECTOR('',#27019,1.);
#3842=VECTOR('',#27020,1.);
#3843=VECTOR('',#27025,1.);
#3844=VECTOR('',#27026,1.);
#3845=VECTOR('',#27027,1.);
#3846=VECTOR('',#27030,1.);
#3847=VECTOR('',#27035,1.);
#3848=VECTOR('',#27036,1.);
#3849=VECTOR('',#27037,1.);
#3850=VECTOR('',#27040,1.);
#3851=VECTOR('',#27043,1.);
#4703=CYLINDRICAL_SURFACE('',#21754,0.0005);
#5588=FACE_OUTER_BOUND('',#6715,.T.);
#5589=FACE_OUTER_BOUND('',#6716,.T.);
#5590=FACE_OUTER_BOUND('',#6717,.T.);
#5591=FACE_OUTER_BOUND('',#6718,.T.);
#5592=FACE_OUTER_BOUND('',#6719,.T.);
#5593=FACE_OUTER_BOUND('',#6720,.T.);
#5594=FACE_OUTER_BOUND('',#6721,.T.);
#5595=FACE_OUTER_BOUND('',#6722,.T.);
#5596=FACE_OUTER_BOUND('',#6723,.T.);
#6715=EDGE_LOOP('',(#17108,#17109,#17110,#17111));
#6716=EDGE_LOOP('',(#17112,#17113,#17114,#17115));
#6717=EDGE_LOOP('',(#17116,#17117,#17118,#17119));
#6718=EDGE_LOOP('',(#17120,#17121,#17122,#17123,#17124,#17125,#17126));
#6719=EDGE_LOOP('',(#17127,#17128,#17129,#17130));
#6720=EDGE_LOOP('',(#17131,#17132,#17133,#17134,#17135,#17136,#17137));
#6721=EDGE_LOOP('',(#17138,#17139,#17140,#17141));
#6722=EDGE_LOOP('',(#17142,#17143,#17144,#17145));
#6723=EDGE_LOOP('',(#17146,#17147,#17148,#17149));
#7859=CIRCLE('',#21753,0.00050000000001);
#7860=CIRCLE('',#21755,0.00050000000001);
#9499=VERTEX_POINT('',#33165);
#9500=VERTEX_POINT('',#33166);
#9501=VERTEX_POINT('',#33168);
#9502=VERTEX_POINT('',#33170);
#9503=VERTEX_POINT('',#33174);
#9504=VERTEX_POINT('',#33175);
#9505=VERTEX_POINT('',#33177);
#9506=VERTEX_POINT('',#33179);
#9507=VERTEX_POINT('',#33186);
#9508=VERTEX_POINT('',#33188);
#9509=VERTEX_POINT('',#33190);
#9510=VERTEX_POINT('',#33194);
#9511=VERTEX_POINT('',#33198);
#9512=VERTEX_POINT('',#33200);
#12112=EDGE_CURVE('',#9499,#9500,#2234,.T.);
#12113=EDGE_CURVE('',#9500,#9501,#2235,.T.);
#12114=EDGE_CURVE('',#9501,#9502,#2236,.T.);
#12115=EDGE_CURVE('',#9499,#9502,#2237,.T.);
#12116=EDGE_CURVE('',#9503,#9504,#2238,.T.);
#12117=EDGE_CURVE('',#9503,#9505,#2239,.T.);
#12118=EDGE_CURVE('',#9505,#9506,#2240,.T.);
#12119=EDGE_CURVE('',#9504,#9506,#2241,.T.);
#12120=EDGE_CURVE('',#9506,#9501,#2242,.T.);
#12121=EDGE_CURVE('',#9502,#9505,#2243,.T.);
#12122=EDGE_CURVE('',#9507,#9504,#7859,.T.);
#12123=EDGE_CURVE('',#9500,#9508,#2244,.T.);
#12124=EDGE_CURVE('',#9509,#9508,#2245,.T.);
#12125=EDGE_CURVE('',#9507,#9509,#2246,.T.);
#12126=EDGE_CURVE('',#9510,#9507,#2247,.T.);
#12127=EDGE_CURVE('',#9510,#9503,#7860,.T.);
#12128=EDGE_CURVE('',#9511,#9510,#2248,.T.);
#12129=EDGE_CURVE('',#9512,#9511,#2249,.T.);
#12130=EDGE_CURVE('',#9499,#9512,#2250,.T.);
#12131=EDGE_CURVE('',#9508,#9512,#2251,.T.);
#12132=EDGE_CURVE('',#9511,#9509,#2252,.T.);
#17108=ORIENTED_EDGE('',*,*,#12112,.T.);
#17109=ORIENTED_EDGE('',*,*,#12113,.T.);
#17110=ORIENTED_EDGE('',*,*,#12114,.T.);
#17111=ORIENTED_EDGE('',*,*,#12115,.F.);
#17112=ORIENTED_EDGE('',*,*,#12116,.F.);
#17113=ORIENTED_EDGE('',*,*,#12117,.T.);
#17114=ORIENTED_EDGE('',*,*,#12118,.T.);
#17115=ORIENTED_EDGE('',*,*,#12119,.F.);
#17116=ORIENTED_EDGE('',*,*,#12114,.F.);
#17117=ORIENTED_EDGE('',*,*,#12120,.F.);
#17118=ORIENTED_EDGE('',*,*,#12118,.F.);
#17119=ORIENTED_EDGE('',*,*,#12121,.F.);
#17120=ORIENTED_EDGE('',*,*,#12122,.T.);
#17121=ORIENTED_EDGE('',*,*,#12119,.T.);
#17122=ORIENTED_EDGE('',*,*,#12120,.T.);
#17123=ORIENTED_EDGE('',*,*,#12113,.F.);
#17124=ORIENTED_EDGE('',*,*,#12123,.T.);
#17125=ORIENTED_EDGE('',*,*,#12124,.F.);
#17126=ORIENTED_EDGE('',*,*,#12125,.F.);
#17127=ORIENTED_EDGE('',*,*,#12126,.F.);
#17128=ORIENTED_EDGE('',*,*,#12127,.T.);
#17129=ORIENTED_EDGE('',*,*,#12116,.T.);
#17130=ORIENTED_EDGE('',*,*,#12122,.F.);
#17131=ORIENTED_EDGE('',*,*,#12115,.T.);
#17132=ORIENTED_EDGE('',*,*,#12121,.T.);
#17133=ORIENTED_EDGE('',*,*,#12117,.F.);
#17134=ORIENTED_EDGE('',*,*,#12127,.F.);
#17135=ORIENTED_EDGE('',*,*,#12128,.F.);
#17136=ORIENTED_EDGE('',*,*,#12129,.F.);
#17137=ORIENTED_EDGE('',*,*,#12130,.F.);
#17138=ORIENTED_EDGE('',*,*,#12130,.T.);
#17139=ORIENTED_EDGE('',*,*,#12131,.F.);
#17140=ORIENTED_EDGE('',*,*,#12123,.F.);
#17141=ORIENTED_EDGE('',*,*,#12112,.F.);
#17142=ORIENTED_EDGE('',*,*,#12125,.T.);
#17143=ORIENTED_EDGE('',*,*,#12132,.F.);
#17144=ORIENTED_EDGE('',*,*,#12128,.T.);
#17145=ORIENTED_EDGE('',*,*,#12126,.T.);
#17146=ORIENTED_EDGE('',*,*,#12132,.T.);
#17147=ORIENTED_EDGE('',*,*,#12124,.T.);
#17148=ORIENTED_EDGE('',*,*,#12131,.T.);
#17149=ORIENTED_EDGE('',*,*,#12129,.T.);
#19304=ADVANCED_FACE('',(#5588),#943,.T.);
#19305=ADVANCED_FACE('',(#5589),#944,.F.);
#19306=ADVANCED_FACE('',(#5590),#945,.F.);
#19307=ADVANCED_FACE('',(#5591),#946,.T.);
#19308=ADVANCED_FACE('',(#5592),#4703,.T.);
#19309=ADVANCED_FACE('',(#5593),#947,.T.);
#19310=ADVANCED_FACE('',(#5594),#948,.T.);
#19311=ADVANCED_FACE('',(#5595),#949,.T.);
#19312=ADVANCED_FACE('',(#5596),#950,.T.);
#19577=CLOSED_SHELL('',(#19304,#19305,#19306,#19307,#19308,#19309,#19310,
#19311,#19312));
#21748=AXIS2_PLACEMENT_3D('',#33163,#27003,#27004);
#21749=AXIS2_PLACEMENT_3D('',#33164,#27005,#27006);
#21750=AXIS2_PLACEMENT_3D('',#33173,#27011,#27012);
#21751=AXIS2_PLACEMENT_3D('',#33182,#27017,#27018);
#21752=AXIS2_PLACEMENT_3D('',#33185,#27021,#27022);
#21753=AXIS2_PLACEMENT_3D('',#33187,#27023,#27024);
#21754=AXIS2_PLACEMENT_3D('',#33193,#27028,#27029);
#21755=AXIS2_PLACEMENT_3D('',#33196,#27031,#27032);
#21756=AXIS2_PLACEMENT_3D('',#33197,#27033,#27034);
#21757=AXIS2_PLACEMENT_3D('',#33203,#27038,#27039);
#21758=AXIS2_PLACEMENT_3D('',#33205,#27041,#27042);
#21759=AXIS2_PLACEMENT_3D('',#33207,#27044,#27045);
#27003=DIRECTION('axis',(0.,0.,1.));
#27004=DIRECTION('refdir',(1.,0.,0.));
#27005=DIRECTION('center_axis',(1.,5.1420277733694E-16,-1.0522467400333E-14));
#27006=DIRECTION('ref_axis',(-1.0522467400333E-14,1.06077175752244E-14,
-1.));
#27007=DIRECTION('',(-1.00001914094642E-12,1.00002200370999E-12,1.));
#27008=DIRECTION('',(-9.47915311079142E-15,-1.,1.E-14));
#27009=DIRECTION('',(1.00001914094642E-12,-9.99999999998997E-13,-1.));
#27010=DIRECTION('',(-9.47915311079142E-15,-1.,1.E-14));
#27011=DIRECTION('center_axis',(1.,5.2084688920845E-16,-1.0522467400333E-14));
#27012=DIRECTION('ref_axis',(-1.0522467400333E-14,1.01548957588061E-14,
-1.));
#27013=DIRECTION('',(-9.56631913100564E-15,9.99999999999985E-15,1.));
#27014=DIRECTION('',(-9.47915311079142E-15,-1.,1.E-14));
#27015=DIRECTION('',(-9.56631913100564E-15,9.99999999999985E-15,1.));
#27016=DIRECTION('',(-9.47915311079142E-15,-1.,1.E-14));
#27017=DIRECTION('center_axis',(-4.5961454925099E-16,1.,6.61092274672771E-17));
#27018=DIRECTION('ref_axis',(-1.05885766278003E-14,6.61092274672722E-17,
-1.));
#27019=DIRECTION('',(1.,-9.54038545074888E-15,9.9999999999998E-15));
#27020=DIRECTION('',(-1.,9.54038545074888E-15,-9.9999999999998E-15));
#27021=DIRECTION('center_axis',(0.,3.71824206197546E-31,1.));
#27022=DIRECTION('ref_axis',(1.,3.89820370584558E-15,-1.44944649852236E-45));
#27023=DIRECTION('center_axis',(-1.99999999991998E-11,2.E-11,1.));
#27024=DIRECTION('ref_axis',(-1.99995712428458E-11,-1.,1.99999999996E-11));
#27025=DIRECTION('',(1.,-9.99466108488984E-13,1.00024333162532E-12));
#27026=DIRECTION('',(-9.99479153109799E-13,-1.,-1.00441888838649E-12));
#27027=DIRECTION('',(1.,-9.99466108488984E-13,1.00024333162532E-12));
#27028=DIRECTION('center_axis',(0.,-4.29362650667545E-31,1.));
#27029=DIRECTION('ref_axis',(4.28756753891971E-16,-1.,-4.29362650667545E-31));
#27030=DIRECTION('',(-9.99999999999976E-15,-1.04336808689941E-14,1.));
#27031=DIRECTION('center_axis',(-1.99999999991998E-11,2.E-11,1.));
#27032=DIRECTION('ref_axis',(-1.99995712428458E-11,-1.,1.99999999996E-11));
#27033=DIRECTION('center_axis',(-1.0522467400333E-14,6.93088260946523E-29,
-1.));
#27034=DIRECTION('ref_axis',(1.,-6.62426369448742E-15,-1.0522467400333E-14));
#27035=DIRECTION('',(-1.,9.99485333130104E-13,-9.99628143109513E-13));
#27036=DIRECTION('',(9.99479153109799E-13,1.,1.00441888838649E-12));
#27037=DIRECTION('',(1.,-9.99466108488984E-13,1.00024333162532E-12));
#27038=DIRECTION('center_axis',(5.33891510011771E-16,-1.,2.20037109950003E-17));
#27039=DIRECTION('ref_axis',(-1.,-5.33891510011771E-16,1.0522467400333E-14));
#27040=DIRECTION('',(9.99999999998993E-13,-1.00002200370999E-12,-1.));
#27041=DIRECTION('center_axis',(-5.3389151001178E-16,1.,6.61092274672815E-17));
#27042=DIRECTION('ref_axis',(-9.50035731417012E-15,6.61092274672764E-17,
-1.));
#27043=DIRECTION('',(-9.99999999998985E-13,-1.00108821931263E-12,1.));
#27044=DIRECTION('center_axis',(1.,5.33891510011885E-16,-1.0522467400333E-14));
#27045=DIRECTION('ref_axis',(-1.0522467400333E-14,1.08319082541355E-14,
-1.));
#33163=CARTESIAN_POINT('',(0.,0.,0.));
#33164=CARTESIAN_POINT('Origin',(0.02115,-0.0223,-0.01175));
#33165=CARTESIAN_POINT('',(0.02115,-0.02545,0.000749999999999928));
#33166=CARTESIAN_POINT('',(0.02115,-0.02545,0.00124999999999993));
#33167=CARTESIAN_POINT('',(0.02115000000001,-0.02545000000001,-0.00549999999999003));
#33168=CARTESIAN_POINT('',(0.02115,-0.0317,0.00124999999999993));
#33169=CARTESIAN_POINT('',(0.02115000000001,-0.02545000000001,0.00125000000000993));
#33170=CARTESIAN_POINT('',(0.02115,-0.0317,0.000749999999999928));
#33171=CARTESIAN_POINT('',(0.0211500000000101,-0.0317000000000099,-0.00549999999999003));
#33172=CARTESIAN_POINT('',(0.0211500000000101,-0.02545000000001,0.000750000000009929));
#33173=CARTESIAN_POINT('Origin',(0.02065,-0.02545,0.00124999999999993));
#33174=CARTESIAN_POINT('',(0.02065,-0.02545,0.000749999999999933));
#33175=CARTESIAN_POINT('',(0.02065,-0.02545,0.00124999999999993));
#33176=CARTESIAN_POINT('',(0.0206500000000101,-0.02545000000001,0.00125000000000993));
#33177=CARTESIAN_POINT('',(0.02065,-0.0317,0.000749999999999933));
#33178=CARTESIAN_POINT('',(0.0206500000000101,-0.02545000000001,0.000750000000009934));
#33179=CARTESIAN_POINT('',(0.02065,-0.0317,0.00124999999999993));
#33180=CARTESIAN_POINT('',(0.0206500000000101,-0.03170000000001,0.00125000000000993));
#33181=CARTESIAN_POINT('',(0.0206500000000101,-0.02545000000001,0.00125000000000993));
#33182=CARTESIAN_POINT('Origin',(0.02115,-0.0317,0.000749999999999928));
#33183=CARTESIAN_POINT('',(0.0206500000000101,-0.03170000000001,0.00125000000000993));
#33184=CARTESIAN_POINT('',(0.0206500000000101,-0.03170000000001,0.000750000000009934));
#33185=CARTESIAN_POINT('Origin',(0.02115,-0.02495,0.00124999999999993));
#33186=CARTESIAN_POINT('',(0.02115,-0.02495,0.00124999999999993));
#33187=CARTESIAN_POINT('Origin',(0.02115000000001,-0.02545000000001,0.00125000000000993));
#33188=CARTESIAN_POINT('',(0.0262,-0.02545,0.00124999999999987));
#33189=CARTESIAN_POINT('',(0.0229000000000101,-0.02545000000001,0.00125000000000991));
#33190=CARTESIAN_POINT('',(0.0262,-0.02495,0.00124999999999987));
#33191=CARTESIAN_POINT('',(0.0262000000000101,-0.02545000000001,0.00125000000000997));
#33192=CARTESIAN_POINT('',(0.0229000000000101,-0.02495000000001,0.00125000000000991));
#33193=CARTESIAN_POINT('Origin',(0.02115,-0.02545,0.000999999999999926));
#33194=CARTESIAN_POINT('',(0.02115,-0.02495,0.000749999999999928));
#33195=CARTESIAN_POINT('',(0.0211500000000101,-0.02495000000001,0.00125000000000993));
#33196=CARTESIAN_POINT('Origin',(0.0211500000000101,-0.02545000000001,0.000750000000009929));
#33197=CARTESIAN_POINT('Origin',(0.02115,-0.02495,0.000749999999999928));
#33198=CARTESIAN_POINT('',(0.0262,-0.02495,0.000749999999999874));
#33199=CARTESIAN_POINT('',(0.0229000000000101,-0.02495000000001,0.000750000000009909));
#33200=CARTESIAN_POINT('',(0.0262,-0.02545,0.000749999999999874));
#33201=CARTESIAN_POINT('',(0.0262000000000101,-0.02495000000001,0.000750000000009974));
#33202=CARTESIAN_POINT('',(0.0229000000000101,-0.02545000000001,0.000750000000009909));
#33203=CARTESIAN_POINT('Origin',(0.0229,-0.02545,0.00124999999999991));
#33204=CARTESIAN_POINT('',(0.0262000000000101,-0.02545000000001,0.000750000000009974));
#33205=CARTESIAN_POINT('Origin',(0.0229,-0.02495,0.000749999999999909));
#33206=CARTESIAN_POINT('',(0.0262000000000101,-0.02495000000001,0.00125000000000997));
#33207=CARTESIAN_POINT('Origin',(0.0262,-0.0252,0.000999999999999873));
#34831=UNCERTAINTY_MEASURE_WITH_UNIT(LENGTH_MEASURE(1.E-5),#34877,
'DISTANCE_ACCURACY_VALUE',
'Maximum model space distance between geometric entities at asserted c
onnectivities');
#34841=UNCERTAINTY_MEASURE_WITH_UNIT(LENGTH_MEASURE(1.E-5),#34877,
'DISTANCE_ACCURACY_VALUE',
'Maximum model space distance between geometric entities at asserted c
onnectivities');
#34866=(
GEOMETRIC_REPRESENTATION_CONTEXT(3)
GLOBAL_UNCERTAINTY_ASSIGNED_CONTEXT((#34831))
GLOBAL_UNIT_ASSIGNED_CONTEXT((#34877,#34878,#34879))
REPRESENTATION_CONTEXT('','3D')
);
#34876=(
GEOMETRIC_REPRESENTATION_CONTEXT(3)
GLOBAL_UNCERTAINTY_ASSIGNED_CONTEXT((#34841))
GLOBAL_UNIT_ASSIGNED_CONTEXT((#34877,#34878,#34879))
REPRESENTATION_CONTEXT('','3D')
);
#34877=(
LENGTH_UNIT()
NAMED_UNIT(*)
SI_UNIT($,.METRE.)
);
#34878=(
NAMED_UNIT(*)
PLANE_ANGLE_UNIT()
SI_UNIT($,.RADIAN.)
);
#34879=(
NAMED_UNIT(*)
SI_UNIT($,.STERADIAN.)
SOLID_ANGLE_UNIT()
);
#34904=SHAPE_DEFINITION_REPRESENTATION(#34938,#35008);
#34938=PRODUCT_DEFINITION_SHAPE('',$,#35043);
#35008=SHAPE_REPRESENTATION('',(#21748),#34866);
#35018=PRODUCT_DEFINITION_CONTEXT('part definition',#35122,'design');
#35043=PRODUCT_DEFINITION('Socket Screw 5','Socket Screw 5',#35077,#35018);
#35077=PRODUCT_DEFINITION_FORMATION('',$,#35148);
#35122=APPLICATION_CONTEXT('Managed model based 3d engineering');
#35123=PRODUCT_CONTEXT('part definition',#35122,'mechanical');
#35148=PRODUCT('Socket Screw 5','Socket Screw 5',
'LEGAL AND USAGE DISCLAIMER: this Data/Model is provided \X2\201C\X0\A
S IS\X2\201D\X0\ for informational and representational only. It is a 
geometric approximation and is NOT engineered, certified, or guarantee
d for dimensional accuracy, exact tolerances, or production-level prec
ision. Vendor disclaims all implied warranties including fitness for a
 particular purpose. DO NOT USE FOR DIRECT PHYSICAL MANUFACTURING, AUT
OMATED PRODUCTION, OR SAFETY-CRITICAL SYSTEMS without independent engi
neering verification and resolution of any design discrepancies.',(#35123));
#35159=PRESENTATION_STYLE_ASSIGNMENT((#35168));
#35168=SURFACE_STYLE_USAGE(.BOTH.,#35177);
#35177=SURFACE_SIDE_STYLE('',(#35186));
#35186=SURFACE_STYLE_FILL_AREA(#35195);
#35195=FILL_AREA_STYLE('Paint - Enamel Glossy (White)',(#35204));
#35204=FILL_AREA_STYLE_COLOUR('Paint - Enamel Glossy (White)',#35213);
#35213=COLOUR_RGB('Paint - Enamel Glossy (White)',0.964705882352941,0.964705882352941,
0.952941176470588);
ENDSEC;
END-ISO-10303-21;
